ISO-10303-21;
HEADER;
/* Generated by software containing ST-Developer
 * from STEP Tools, Inc. (www.steptools.com) 
 */

FILE_DESCRIPTION(
/* description */ ('CAx-IF Rec.Pracs.---Representation and Presentation of Product Manufa
cturing Information (PMI)---4.0---2014-10-13'),
/* implementation_level */ '2;1');

FILE_NAME(
/* name */ 'Socket Screw 2.step',
/* time_stamp */ '2026-10-24T18:52:33-07:00',
/* author */ (''),
/* organization */ (''),
/* preprocessor_version */ 'ST-DEVELOPER v20.2',
/* originating_system */ 'Autodesk Translation Framework v15.17.0.0',
/* authorisation */ '');

FILE_SCHEMA (('AP242_MANAGED_MODEL_BASED_3D_ENGINEERING_MIM_LF { 1 0 10303 442 2 1 4 }'));
ENDSEC;

DATA;
#10=MECHANICAL_DESIGN_GEOMETRIC_PRESENTATION_REPRESENTATION('',(#422),#34876);
#356=SHAPE_REPRESENTATION_RELATIONSHIP('SRR','None',#34993,#389);
#389=ADVANCED_BREP_SHAPE_REPRESENTATION('',(#455),#34851);
#422=STYLED_ITEM('',(#35165),#455);
#455=MANIFOLD_SOLID_BREP('Socket Screw 2',#19562);
#786=PLANE('',#20822);
#787=PLANE('',#20823);
#788=PLANE('',#20827);
#789=PLANE('',#20828);
#790=PLANE('',#20829);
#791=PLANE('',#20830);
#792=PLANE('',#20831);
#793=PLANE('',#20832);
#1658=LINE('',#30937,#3257);
#1659=LINE('',#30939,#3258);
#1660=LINE('',#30941,#3259);
#1661=LINE('',#30942,#3260);
#1662=LINE('',#30947,#3261);
#1663=LINE('',#30949,#3262);
#1664=LINE('',#30951,#3263);
#1665=LINE('',#30953,#3264);
#1666=LINE('',#30954,#3265);
#1667=LINE('',#30957,#3266);
#1668=LINE('',#30962,#3267);
#1669=LINE('',#30963,#3268);
#1670=LINE('',#30965,#3269);
#1671=LINE('',#30967,#3270);
#1672=LINE('',#30968,#3271);
#1673=LINE('',#30970,#3272);
#1674=LINE('',#30972,#3273);
#1675=LINE('',#30974,#3274);
#1676=LINE('',#30976,#3275);
#3257=VECTOR('',#24577,1.);
#3258=VECTOR('',#24578,1.);
#3259=VECTOR('',#24579,1.);
#3260=VECTOR('',#24580,1.);
#3261=VECTOR('',#24585,1.);
#3262=VECTOR('',#24586,1.);
#3263=VECTOR('',#24587,1.);
#3264=VECTOR('',#24588,1.);
#3265=VECTOR('',#24589,1.);
#3266=VECTOR('',#24592,1.);
#3267=VECTOR('',#24597,1.);
#3268=VECTOR('',#24598,1.);
#3269=VECTOR('',#24599,1.);
#3270=VECTOR('',#24600,1.);
#3271=VECTOR('',#24601,1.);
#3272=VECTOR('',#24604,1.);
#3273=VECTOR('',#24607,1.);
#3274=VECTOR('',#24610,1.);
#3275=VECTOR('',#24613,1.);
#4467=CYLINDRICAL_SURFACE('',#20825,0.0005);
#5185=FACE_OUTER_BOUND('',#6269,.T.);
#5186=FACE_OUTER_BOUND('',#6270,.T.);
#5187=FACE_OUTER_BOUND('',#6271,.T.);
#5188=FACE_OUTER_BOUND('',#6272,.T.);
#5189=FACE_OUTER_BOUND('',#6273,.T.);
#5190=FACE_OUTER_BOUND('',#6274,.T.);
#5191=FACE_OUTER_BOUND('',#6275,.T.);
#5192=FACE_OUTER_BOUND('',#6276,.T.);
#5193=FACE_OUTER_BOUND('',#6277,.T.);
#6269=EDGE_LOOP('',(#14934,#14935,#14936,#14937));
#6270=EDGE_LOOP('',(#14938,#14939,#14940,#14941,#14942,#14943,#14944));
#6271=EDGE_LOOP('',(#14945,#14946,#14947,#14948));
#6272=EDGE_LOOP('',(#14949,#14950,#14951,#14952,#14953,#14954,#14955));
#6273=EDGE_LOOP('',(#14956,#14957,#14958,#14959));
#6274=EDGE_LOOP('',(#14960,#14961,#14962,#14963));
#6275=EDGE_LOOP('',(#14964,#14965,#14966,#14967));
#6276=EDGE_LOOP('',(#14968,#14969,#14970,#14971));
#6277=EDGE_LOOP('',(#14972,#14973,#14974,#14975));
#7374=CIRCLE('',#20824,0.00050000000001);
#7375=CIRCLE('',#20826,0.00050000000001);
#8778=VERTEX_POINT('',#30935);
#8779=VERTEX_POINT('',#30936);
#8780=VERTEX_POINT('',#30938);
#8781=VERTEX_POINT('',#30940);
#8782=VERTEX_POINT('',#30944);
#8783=VERTEX_POINT('',#30946);
#8784=VERTEX_POINT('',#30948);
#8785=VERTEX_POINT('',#30950);
#8786=VERTEX_POINT('',#30952);
#8787=VERTEX_POINT('',#30956);
#8788=VERTEX_POINT('',#30960);
#8789=VERTEX_POINT('',#30961);
#8790=VERTEX_POINT('',#30964);
#8791=VERTEX_POINT('',#30966);
#11025=EDGE_CURVE('',#8778,#8779,#1658,.T.);
#11026=EDGE_CURVE('',#8778,#8780,#1659,.T.);
#11027=EDGE_CURVE('',#8780,#8781,#1660,.T.);
#11028=EDGE_CURVE('',#8779,#8781,#1661,.T.);
#11029=EDGE_CURVE('',#8782,#8779,#7374,.T.);
#11030=EDGE_CURVE('',#8781,#8783,#1662,.T.);
#11031=EDGE_CURVE('',#8784,#8783,#1663,.T.);
#11032=EDGE_CURVE('',#8784,#8785,#1664,.T.);
#11033=EDGE_CURVE('',#8786,#8785,#1665,.T.);
#11034=EDGE_CURVE('',#8782,#8786,#1666,.T.);
#11035=EDGE_CURVE('',#8787,#8782,#1667,.T.);
#11036=EDGE_CURVE('',#8787,#8778,#7375,.T.);
#11037=EDGE_CURVE('',#8788,#8789,#1668,.T.);
#11038=EDGE_CURVE('',#8789,#8780,#1669,.T.);
#11039=EDGE_CURVE('',#8790,#8787,#1670,.T.);
#11040=EDGE_CURVE('',#8791,#8790,#1671,.T.);
#11041=EDGE_CURVE('',#8788,#8791,#1672,.T.);
#11042=EDGE_CURVE('',#8783,#8789,#1673,.T.);
#11043=EDGE_CURVE('',#8788,#8784,#1674,.T.);
#11044=EDGE_CURVE('',#8785,#8791,#1675,.T.);
#11045=EDGE_CURVE('',#8790,#8786,#1676,.T.);
#14934=ORIENTED_EDGE('',*,*,#11025,.F.);
#14935=ORIENTED_EDGE('',*,*,#11026,.T.);
#14936=ORIENTED_EDGE('',*,*,#11027,.T.);
#14937=ORIENTED_EDGE('',*,*,#11028,.F.);
#14938=ORIENTED_EDGE('',*,*,#11029,.T.);
#14939=ORIENTED_EDGE('',*,*,#11028,.T.);
#14940=ORIENTED_EDGE('',*,*,#11030,.T.);
#14941=ORIENTED_EDGE('',*,*,#11031,.F.);
#14942=ORIENTED_EDGE('',*,*,#11032,.T.);
#14943=ORIENTED_EDGE('',*,*,#11033,.F.);
#14944=ORIENTED_EDGE('',*,*,#11034,.F.);
#14945=ORIENTED_EDGE('',*,*,#11035,.F.);
#14946=ORIENTED_EDGE('',*,*,#11036,.T.);
#14947=ORIENTED_EDGE('',*,*,#11025,.T.);
#14948=ORIENTED_EDGE('',*,*,#11029,.F.);
#14949=ORIENTED_EDGE('',*,*,#11037,.T.);
#14950=ORIENTED_EDGE('',*,*,#11038,.T.);
#14951=ORIENTED_EDGE('',*,*,#11026,.F.);
#14952=ORIENTED_EDGE('',*,*,#11036,.F.);
#14953=ORIENTED_EDGE('',*,*,#11039,.F.);
#14954=ORIENTED_EDGE('',*,*,#11040,.F.);
#14955=ORIENTED_EDGE('',*,*,#11041,.F.);
#14956=ORIENTED_EDGE('',*,*,#11042,.F.);
#14957=ORIENTED_EDGE('',*,*,#11030,.F.);
#14958=ORIENTED_EDGE('',*,*,#11027,.F.);
#14959=ORIENTED_EDGE('',*,*,#11038,.F.);
#14960=ORIENTED_EDGE('',*,*,#11043,.T.);
#14961=ORIENTED_EDGE('',*,*,#11031,.T.);
#14962=ORIENTED_EDGE('',*,*,#11042,.T.);
#14963=ORIENTED_EDGE('',*,*,#11037,.F.);
#14964=ORIENTED_EDGE('',*,*,#11041,.T.);
#14965=ORIENTED_EDGE('',*,*,#11044,.F.);
#14966=ORIENTED_EDGE('',*,*,#11032,.F.);
#14967=ORIENTED_EDGE('',*,*,#11043,.F.);
#14968=ORIENTED_EDGE('',*,*,#11034,.T.);
#14969=ORIENTED_EDGE('',*,*,#11045,.F.);
#14970=ORIENTED_EDGE('',*,*,#11039,.T.);
#14971=ORIENTED_EDGE('',*,*,#11035,.T.);
#14972=ORIENTED_EDGE('',*,*,#11045,.T.);
#14973=ORIENTED_EDGE('',*,*,#11033,.T.);
#14974=ORIENTED_EDGE('',*,*,#11044,.T.);
#14975=ORIENTED_EDGE('',*,*,#11040,.T.);
#18901=ADVANCED_FACE('',(#5185),#786,.F.);
#18902=ADVANCED_FACE('',(#5186),#787,.T.);
#18903=ADVANCED_FACE('',(#5187),#4467,.T.);
#18904=ADVANCED_FACE('',(#5188),#788,.T.);
#18905=ADVANCED_FACE('',(#5189),#789,.F.);
#18906=ADVANCED_FACE('',(#5190),#790,.T.);
#18907=ADVANCED_FACE('',(#5191),#791,.T.);
#18908=ADVANCED_FACE('',(#5192),#792,.T.);
#18909=ADVANCED_FACE('',(#5193),#793,.T.);
#19562=CLOSED_SHELL('',(#18901,#18902,#18903,#18904,#18905,#18906,#18907,
#18908,#18909));
#20821=AXIS2_PLACEMENT_3D('',#30933,#24573,#24574);
#20822=AXIS2_PLACEMENT_3D('',#30934,#24575,#24576);
#20823=AXIS2_PLACEMENT_3D('',#30943,#24581,#24582);
#20824=AXIS2_PLACEMENT_3D('',#30945,#24583,#24584);
#20825=AXIS2_PLACEMENT_3D('',#30955,#24590,#24591);
#20826=AXIS2_PLACEMENT_3D('',#30958,#24593,#24594);
#20827=AXIS2_PLACEMENT_3D('',#30959,#24595,#24596);
#20828=AXIS2_PLACEMENT_3D('',#30969,#24602,#24603);
#20829=AXIS2_PLACEMENT_3D('',#30971,#24605,#24606);
#20830=AXIS2_PLACEMENT_3D('',#30973,#24608,#24609);
#20831=AXIS2_PLACEMENT_3D('',#30975,#24611,#24612);
#20832=AXIS2_PLACEMENT_3D('',#30977,#24614,#24615);
#24573=DIRECTION('axis',(0.,0.,1.));
#24574=DIRECTION('refdir',(1.,0.,0.));
#24575=DIRECTION('center_axis',(1.,5.2084688920845E-16,-1.0522467400333E-14));
#24576=DIRECTION('ref_axis',(-1.0522467400333E-14,1.01548957588061E-14,
-1.));
#24577=DIRECTION('',(-9.56631913100564E-15,9.99999999999985E-15,1.));
#24578=DIRECTION('',(-9.47915311079142E-15,-1.,1.E-14));
#24579=DIRECTION('',(-9.56631913100564E-15,9.99999999999985E-15,1.));
#24580=DIRECTION('',(-9.47915311079142E-15,-1.,1.E-14));
#24581=DIRECTION('center_axis',(0.,3.71824206197546E-31,1.));
#24582=DIRECTION('ref_axis',(1.,3.89820370584558E-15,-1.44944649852236E-45));
#24583=DIRECTION('center_axis',(-1.99999999991998E-11,2.E-11,1.));
#24584=DIRECTION('ref_axis',(-1.99995712428458E-11,-1.,1.99999999996E-11));
#24585=DIRECTION('',(1.,-9.54038545074888E-15,9.9999999999998E-15));
#24586=DIRECTION('',(-9.47915311079142E-15,-1.,1.E-14));
#24587=DIRECTION('',(1.,-9.99466108488984E-13,1.00024333162532E-12));
#24588=DIRECTION('',(-9.99479153109778E-13,-1.,1.0044628958085E-12));
#24589=DIRECTION('',(1.,-9.99466108488984E-13,1.00024333162532E-12));
#24590=DIRECTION('center_axis',(0.,-4.29362650667545E-31,1.));
#24591=DIRECTION('ref_axis',(4.28756753891971E-16,-1.,-4.29362650667545E-31));
#24592=DIRECTION('',(-9.99999999999976E-15,-1.04336808689941E-14,1.));
#24593=DIRECTION('center_axis',(-1.99999999991998E-11,2.E-11,1.));
#24594=DIRECTION('ref_axis',(-1.99995712428458E-11,-1.,1.99999999996E-11));
#24595=DIRECTION('center_axis',(-1.0522467400333E-14,6.93088260946523E-29,
-1.));
#24596=DIRECTION('ref_axis',(1.,-6.62426369448742E-15,-1.0522467400333E-14));
#24597=DIRECTION('',(-9.47915311079142E-15,-1.,1.E-14));
#24598=DIRECTION('',(-1.,9.54038545074888E-15,-9.9999999999998E-15));
#24599=DIRECTION('',(-1.,9.99485333130104E-13,-9.99628143109513E-13));
#24600=DIRECTION('',(9.99479153109778E-13,1.,-1.00002200371E-12));
#24601=DIRECTION('',(1.,-9.99466108488984E-13,1.00024333162532E-12));
#24602=DIRECTION('center_axis',(-4.5961454925099E-16,1.,6.61092274672771E-17));
#24603=DIRECTION('ref_axis',(-1.05885766278003E-14,6.61092274672722E-17,
-1.));
#24604=DIRECTION('',(1.00001914094642E-12,-9.99999999998997E-13,-1.));
#24605=DIRECTION('center_axis',(1.,5.1420277733694E-16,-1.0522467400333E-14));
#24606=DIRECTION('ref_axis',(-1.0522467400333E-14,1.06077175752244E-14,
-1.));
#24607=DIRECTION('',(-1.00001914094642E-12,1.00002200370999E-12,1.));
#24608=DIRECTION('center_axis',(5.33891510011771E-16,-1.,2.20037109950003E-17));
#24609=DIRECTION('ref_axis',(-1.,-5.33891510011771E-16,1.0522467400333E-14));
#24610=DIRECTION('',(9.99999999998993E-13,-1.00002200370999E-12,-1.));
#24611=DIRECTION('center_axis',(-5.3389151001177E-16,1.,6.61092274672778E-17));
#24612=DIRECTION('ref_axis',(-1.06105803387953E-14,6.61092274672721E-17,
-1.));
#24613=DIRECTION('',(-9.99999999998993E-13,1.00002200370999E-12,1.));
#24614=DIRECTION('center_axis',(1.,5.33891510011885E-16,-1.0522467400333E-14));
#24615=DIRECTION('ref_axis',(-1.0522467400333E-14,1.08319082541355E-14,
-1.));
#30933=CARTESIAN_POINT('',(0.,0.,0.));
#30934=CARTESIAN_POINT('Origin',(0.02065,-0.02545,0.00324999999999993));
#30935=CARTESIAN_POINT('',(0.02065,-0.02545,0.00274999999999993));
#30936=CARTESIAN_POINT('',(0.02065,-0.02545,0.00324999999999993));
#30937=CARTESIAN_POINT('',(0.0206500000000101,-0.02545000000001,0.00325000000000994));
#30938=CARTESIAN_POINT('',(0.02065,-0.0317,0.00274999999999993));
#30939=CARTESIAN_POINT('',(0.0206500000000101,-0.02545000000001,0.00275000000000994));
#30940=CARTESIAN_POINT('',(0.02065,-0.0317,0.00324999999999993));
#30941=CARTESIAN_POINT('',(0.0206500000000101,-0.03170000000001,0.00325000000000994));
#30942=CARTESIAN_POINT('',(0.0206500000000101,-0.02545000000001,0.00325000000000994));
#30943=CARTESIAN_POINT('Origin',(0.02115,-0.02495,0.00324999999999992));
#30944=CARTESIAN_POINT('',(0.02115,-0.02495,0.00324999999999992));
#30945=CARTESIAN_POINT('Origin',(0.02115000000001,-0.02545000000001,0.00325000000000992));
#30946=CARTESIAN_POINT('',(0.02115,-0.0317,0.00324999999999992));
#30947=CARTESIAN_POINT('',(0.0206500000000101,-0.03170000000001,0.00325000000000994));
#30948=CARTESIAN_POINT('',(0.02115,-0.02545,0.00324999999999992));
#30949=CARTESIAN_POINT('',(0.02115000000001,-0.02545000000001,0.00325000000000992));
#30950=CARTESIAN_POINT('',(0.0262,-0.02545,0.00324999999999987));
#30951=CARTESIAN_POINT('',(0.0229000000000101,-0.02545000000001,0.00325000000000991));
#30952=CARTESIAN_POINT('',(0.0262,-0.02495,0.00324999999999987));
#30953=CARTESIAN_POINT('',(0.0262000000000101,-0.02545000000001,0.00325000000000997));
#30954=CARTESIAN_POINT('',(0.0229000000000101,-0.02495000000001,0.00325000000000991));
#30955=CARTESIAN_POINT('Origin',(0.02115,-0.02545,0.00299999999999993));
#30956=CARTESIAN_POINT('',(0.02115,-0.02495,0.00274999999999993));
#30957=CARTESIAN_POINT('',(0.0211500000000101,-0.02495000000001,0.00325000000000992));
#30958=CARTESIAN_POINT('Origin',(0.0211500000000101,-0.02545000000001,0.00275000000000993));
#30959=CARTESIAN_POINT('Origin',(0.02115,-0.02495,0.00274999999999993));
#30960=CARTESIAN_POINT('',(0.02115,-0.02545,0.00274999999999993));
#30961=CARTESIAN_POINT('',(0.02115,-0.0317,0.00274999999999993));
#30962=CARTESIAN_POINT('',(0.0211500000000101,-0.02545000000001,0.00275000000000993));
#30963=CARTESIAN_POINT('',(0.0206500000000101,-0.03170000000001,0.00275000000000994));
#30964=CARTESIAN_POINT('',(0.0262,-0.02495,0.00274999999999987));
#30965=CARTESIAN_POINT('',(0.0229000000000101,-0.02495000000001,0.00275000000000991));
#30966=CARTESIAN_POINT('',(0.0262,-0.02545,0.00274999999999987));
#30967=CARTESIAN_POINT('',(0.0262000000000101,-0.02495000000001,0.00275000000000997));
#30968=CARTESIAN_POINT('',(0.0229000000000101,-0.02545000000001,0.00275000000000991));
#30969=CARTESIAN_POINT('Origin',(0.02115,-0.0317,0.000749999999999928));
#30970=CARTESIAN_POINT('',(0.0211500000000101,-0.0317000000000099,-0.00549999999999003));
#30971=CARTESIAN_POINT('Origin',(0.02115,-0.0223,-0.01175));
#30972=CARTESIAN_POINT('',(0.0211500000000101,-0.02545000000001,-0.00449999999999003));
#30973=CARTESIAN_POINT('Origin',(0.0229,-0.02545,0.00324999999999991));
#30974=CARTESIAN_POINT('',(0.0262000000000101,-0.02545000000001,0.00275000000000997));
#30975=CARTESIAN_POINT('Origin',(0.0229,-0.02495,0.00274999999999991));
#30976=CARTESIAN_POINT('',(0.0262000000000101,-0.02495000000001,0.00325000000000997));
#30977=CARTESIAN_POINT('Origin',(0.0262,-0.0252,0.00299999999999988));
#34816=UNCERTAINTY_MEASURE_WITH_UNIT(LENGTH_MEASURE(1.E-5),#34877,
'DISTANCE_ACCURACY_VALUE',
'Maximum model space distance between geometric entities at asserted c
onnectivities');
#34841=UNCERTAINTY_MEASURE_WITH_UNIT(LENGTH_MEASURE(1.E-5),#34877,
'DISTANCE_ACCURACY_VALUE',
'Maximum model space distance between geometric entities at asserted c
onnectivities');
#34851=(
GEOMETRIC_REPRESENTATION_CONTEXT(3)
GLOBAL_UNCERTAINTY_ASSIGNED_CONTEXT((#34816))
GLOBAL_UNIT_ASSIGNED_CONTEXT((#34877,#34878,#34879))
REPRESENTATION_CONTEXT('','3D')
);
#34876=(
GEOMETRIC_REPRESENTATION_CONTEXT(3)
GLOBAL_UNCERTAINTY_ASSIGNED_CONTEXT((#34841))
GLOBAL_UNIT_ASSIGNED_CONTEXT((#34877,#34878,#34879))
REPRESENTATION_CONTEXT('','3D')
);
#34877=(
LENGTH_UNIT()
NAMED_UNIT(*)
SI_UNIT($,.METRE.)
);
#34878=(
NAMED_UNIT(*)
PLANE_ANGLE_UNIT()
SI_UNIT($,.RADIAN.)
);
#34879=(
NAMED_UNIT(*)
SI_UNIT($,.STERADIAN.)
SOLID_ANGLE_UNIT()
);
#34889=SHAPE_DEFINITION_REPRESENTATION(#34923,#34993);
#34923=PRODUCT_DEFINITION_SHAPE('',$,#35028);
#34993=SHAPE_REPRESENTATION('',(#20821),#34851);
#35018=PRODUCT_DEFINITION_CONTEXT('part definition',#35122,'design');
#35028=PRODUCT_DEFINITION('Socket Screw 2','Socket Screw 2',#35062,#35018);
#35062=PRODUCT_DEFINITION_FORMATION('',$,#35133);
#35122=APPLICATION_CONTEXT('Managed model based 3d engineering');
#35123=PRODUCT_CONTEXT('part definition',#35122,'mechanical');
#35133=PRODUCT('Socket Screw 2','Socket Screw 2',
'LEGAL AND USAGE DISCLAIMER: this Data/Model is provided \X2\201C\X0\A
S IS\X2\201D\X0\ for informational and representational only. It is a 
geometric approximation and is NOT engineered, certified, or guarantee
d for dimensional accuracy, exact tolerances, or production-level prec
ision. Vendor disclaims all implied warranties including fitness for a
 particular purpose. DO NOT USE FOR DIRECT PHYSICAL MANUFACTURING, AUT
OMATED PRODUCTION, OR SAFETY-CRITICAL SYSTEMS without independent engi
neering verification and resolution of any design discrepancies.',(#35123));
#35165=PRESENTATION_STYLE_ASSIGNMENT((#35174));
#35174=SURFACE_STYLE_USAGE(.BOTH.,#35183);
#35183=SURFACE_SIDE_STYLE('',(#35192));
#35192=SURFACE_STYLE_FILL_AREA(#35201);
#35201=FILL_AREA_STYLE('Paint - Metallic (Blue)',(#35210));
#35210=FILL_AREA_STYLE_COLOUR('Paint - Metallic (Blue)',#35219);
#35219=COLOUR_RGB('Paint - Metallic (Blue)',0.188235294117647,0.231372549019608,
0.588235294117647);
ENDSEC;
END-ISO-10303-21;
